ISO-10303-21;
HEADER;
/* Generated by software containing ST-Developer
 * from STEP Tools, Inc. (www.steptools.com) 
 */

FILE_DESCRIPTION(
/* description */ ('Hand drill press frame (manual)'),
/* implementation_level */ '2;1');

FILE_NAME(
/* name */ 'Socket Set Screw - M4x6.step',
/* time_stamp */ '2026-10-28T03:25:28-07:00',
/* author */ (''),
/* organization */ (''),
/* preprocessor_version */ 'ST-DEVELOPER v20.2',
/* originating_system */ 'Autodesk Translation Framework v15.17.0.0',
/* authorisation */ '');

FILE_SCHEMA (('AUTOMOTIVE_DESIGN { 1 0 10303 214 3 1 1 }'));
ENDSEC;

DATA;
#10=MECHANICAL_DESIGN_GEOMETRIC_PRESENTATION_REPRESENTATION('',(#654),#33299);
#481=CONICAL_SURFACE('',#13991,0.185,0.785398163397449);
#482=CONICAL_SURFACE('',#13995,0.1625,0.785398163397449);
#557=SHAPE_REPRESENTATION_RELATIONSHIP('SRR','None',#33518,#602);
#602=ADVANCED_BREP_SHAPE_REPRESENTATION('',(#705),#33280);
#654=STYLED_ITEM('',(#33821),#705);
#705=MANIFOLD_SOLID_BREP('Body1',#12673);
#854=FACE_BOUND('',#2647,.T.);
#1229=PLANE('',#13982);
#1230=PLANE('',#13983);
#1231=PLANE('',#13984);
#1232=PLANE('',#13985);
#1233=PLANE('',#13986);
#1234=PLANE('',#13987);
#1235=PLANE('',#13988);
#1236=PLANE('',#13989);
#1237=PLANE('',#13997);
#1816=FACE_OUTER_BOUND('',#2639,.T.);
#1817=FACE_OUTER_BOUND('',#2640,.T.);
#1818=FACE_OUTER_BOUND('',#2641,.T.);
#1819=FACE_OUTER_BOUND('',#2642,.T.);
#1820=FACE_OUTER_BOUND('',#2643,.T.);
#1821=FACE_OUTER_BOUND('',#2644,.T.);
#1822=FACE_OUTER_BOUND('',#2645,.T.);
#1823=FACE_OUTER_BOUND('',#2646,.T.);
#1824=FACE_OUTER_BOUND('',#2648,.T.);
#1825=FACE_OUTER_BOUND('',#2649,.T.);
#1826=FACE_OUTER_BOUND('',#2650,.T.);
#1827=FACE_OUTER_BOUND('',#2651,.T.);
#2639=EDGE_LOOP('',(#10815,#10816,#10817,#10818));
#2640=EDGE_LOOP('',(#10819,#10820,#10821,#10822));
#2641=EDGE_LOOP('',(#10823,#10824,#10825,#10826));
#2642=EDGE_LOOP('',(#10827,#10828,#10829,#10830));
#2643=EDGE_LOOP('',(#10831,#10832,#10833,#10834));
#2644=EDGE_LOOP('',(#10835,#10836,#10837,#10838));
#2645=EDGE_LOOP('',(#10839,#10840,#10841,#10842,#10843,#10844));
#2646=EDGE_LOOP('',(#10845));
#2647=EDGE_LOOP('',(#10846,#10847,#10848,#10849,#10850,#10851));
#2648=EDGE_LOOP('',(#10852,#10853,#10854,#10855));
#2649=EDGE_LOOP('',(#10856,#10857,#10858,#10859));
#2650=EDGE_LOOP('',(#10860,#10861,#10862,#10863));
#2651=EDGE_LOOP('',(#10864));
#3764=LINE('',#21009,#4929);
#3765=LINE('',#21011,#4930);
#3766=LINE('',#21013,#4931);
#3767=LINE('',#21014,#4932);
#3768=LINE('',#21017,#4933);
#3769=LINE('',#21019,#4934);
#3770=LINE('',#21020,#4935);
#3771=LINE('',#21023,#4936);
#3772=LINE('',#21025,#4937);
#3773=LINE('',#21026,#4938);
#3774=LINE('',#21029,#4939);
#3775=LINE('',#21031,#4940);
#3776=LINE('',#21032,#4941);
#3777=LINE('',#21035,#4942);
#3778=LINE('',#21037,#4943);
#3779=LINE('',#21038,#4944);
#3780=LINE('',#21040,#4945);
#3781=LINE('',#21041,#4946);
#3782=LINE('',#21049,#4947);
#3783=LINE('',#21053,#4948);
#3784=LINE('',#21057,#4949);
#4929=VECTOR('',#16837,1.);
#4930=VECTOR('',#16838,1.);
#4931=VECTOR('',#16839,1.);
#4932=VECTOR('',#16840,1.);
#4933=VECTOR('',#16843,1.);
#4934=VECTOR('',#16844,1.);
#4935=VECTOR('',#16845,1.);
#4936=VECTOR('',#16848,1.);
#4937=VECTOR('',#16849,1.);
#4938=VECTOR('',#16850,1.);
#4939=VECTOR('',#16853,1.);
#4940=VECTOR('',#16854,1.);
#4941=VECTOR('',#16855,1.);
#4942=VECTOR('',#16858,1.);
#4943=VECTOR('',#16859,1.);
#4944=VECTOR('',#16860,1.);
#4945=VECTOR('',#16863,1.);
#4946=VECTOR('',#16864,1.);
#4947=VECTOR('',#16875,0.185);
#4948=VECTOR('',#16880,0.2);
#4949=VECTOR('',#16885,0.1625);
#5493=CIRCLE('',#13990,0.17);
#5494=CIRCLE('',#13992,0.1954);
#5495=CIRCLE('',#13994,0.1954);
#5496=CIRCLE('',#13996,0.125);
#6419=VERTEX_POINT('',#21007);
#6420=VERTEX_POINT('',#21008);
#6421=VERTEX_POINT('',#21010);
#6422=VERTEX_POINT('',#21012);
#6423=VERTEX_POINT('',#21016);
#6424=VERTEX_POINT('',#21018);
#6425=VERTEX_POINT('',#21022);
#6426=VERTEX_POINT('',#21024);
#6427=VERTEX_POINT('',#21028);
#6428=VERTEX_POINT('',#21030);
#6429=VERTEX_POINT('',#21034);
#6430=VERTEX_POINT('',#21036);
#6431=VERTEX_POINT('',#21044);
#6432=VERTEX_POINT('',#21047);
#6433=VERTEX_POINT('',#21051);
#6434=VERTEX_POINT('',#21055);
#7936=EDGE_CURVE('',#6419,#6420,#3764,.T.);
#7937=EDGE_CURVE('',#6419,#6421,#3765,.T.);
#7938=EDGE_CURVE('',#6421,#6422,#3766,.T.);
#7939=EDGE_CURVE('',#6420,#6422,#3767,.T.);
#7940=EDGE_CURVE('',#6423,#6419,#3768,.T.);
#7941=EDGE_CURVE('',#6423,#6424,#3769,.T.);
#7942=EDGE_CURVE('',#6424,#6421,#3770,.T.);
#7943=EDGE_CURVE('',#6425,#6423,#3771,.T.);
#7944=EDGE_CURVE('',#6425,#6426,#3772,.T.);
#7945=EDGE_CURVE('',#6426,#6424,#3773,.T.);
#7946=EDGE_CURVE('',#6427,#6425,#3774,.T.);
#7947=EDGE_CURVE('',#6427,#6428,#3775,.T.);
#7948=EDGE_CURVE('',#6428,#6426,#3776,.T.);
#7949=EDGE_CURVE('',#6429,#6427,#3777,.T.);
#7950=EDGE_CURVE('',#6429,#6430,#3778,.T.);
#7951=EDGE_CURVE('',#6430,#6428,#3779,.T.);
#7952=EDGE_CURVE('',#6420,#6429,#3780,.T.);
#7953=EDGE_CURVE('',#6422,#6430,#3781,.T.);
#7954=EDGE_CURVE('',#6431,#6431,#5493,.T.);
#7955=EDGE_CURVE('',#6432,#6432,#5494,.T.);
#7956=EDGE_CURVE('',#6432,#6431,#3782,.T.);
#7957=EDGE_CURVE('',#6433,#6433,#5495,.F.);
#7958=EDGE_CURVE('',#6433,#6432,#3783,.T.);
#7959=EDGE_CURVE('',#6434,#6434,#5496,.T.);
#7960=EDGE_CURVE('',#6434,#6433,#3784,.T.);
#10815=ORIENTED_EDGE('',*,*,#7936,.F.);
#10816=ORIENTED_EDGE('',*,*,#7937,.T.);
#10817=ORIENTED_EDGE('',*,*,#7938,.T.);
#10818=ORIENTED_EDGE('',*,*,#7939,.F.);
#10819=ORIENTED_EDGE('',*,*,#7940,.F.);
#10820=ORIENTED_EDGE('',*,*,#7941,.T.);
#10821=ORIENTED_EDGE('',*,*,#7942,.T.);
#10822=ORIENTED_EDGE('',*,*,#7937,.F.);
#10823=ORIENTED_EDGE('',*,*,#7943,.F.);
#10824=ORIENTED_EDGE('',*,*,#7944,.T.);
#10825=ORIENTED_EDGE('',*,*,#7945,.T.);
#10826=ORIENTED_EDGE('',*,*,#7941,.F.);
#10827=ORIENTED_EDGE('',*,*,#7946,.F.);
#10828=ORIENTED_EDGE('',*,*,#7947,.T.);
#10829=ORIENTED_EDGE('',*,*,#7948,.T.);
#10830=ORIENTED_EDGE('',*,*,#7944,.F.);
#10831=ORIENTED_EDGE('',*,*,#7949,.F.);
#10832=ORIENTED_EDGE('',*,*,#7950,.T.);
#10833=ORIENTED_EDGE('',*,*,#7951,.T.);
#10834=ORIENTED_EDGE('',*,*,#7947,.F.);
#10835=ORIENTED_EDGE('',*,*,#7952,.F.);
#10836=ORIENTED_EDGE('',*,*,#7939,.T.);
#10837=ORIENTED_EDGE('',*,*,#7953,.T.);
#10838=ORIENTED_EDGE('',*,*,#7950,.F.);
#10839=ORIENTED_EDGE('',*,*,#7953,.F.);
#10840=ORIENTED_EDGE('',*,*,#7938,.F.);
#10841=ORIENTED_EDGE('',*,*,#7942,.F.);
#10842=ORIENTED_EDGE('',*,*,#7945,.F.);
#10843=ORIENTED_EDGE('',*,*,#7948,.F.);
#10844=ORIENTED_EDGE('',*,*,#7951,.F.);
#10845=ORIENTED_EDGE('',*,*,#7954,.F.);
#10846=ORIENTED_EDGE('',*,*,#7936,.T.);
#10847=ORIENTED_EDGE('',*,*,#7952,.T.);
#10848=ORIENTED_EDGE('',*,*,#7949,.T.);
#10849=ORIENTED_EDGE('',*,*,#7946,.T.);
#10850=ORIENTED_EDGE('',*,*,#7943,.T.);
#10851=ORIENTED_EDGE('',*,*,#7940,.T.);
#10852=ORIENTED_EDGE('',*,*,#7955,.F.);
#10853=ORIENTED_EDGE('',*,*,#7956,.T.);
#10854=ORIENTED_EDGE('',*,*,#7954,.T.);
#10855=ORIENTED_EDGE('',*,*,#7956,.F.);
#10856=ORIENTED_EDGE('',*,*,#7957,.F.);
#10857=ORIENTED_EDGE('',*,*,#7958,.T.);
#10858=ORIENTED_EDGE('',*,*,#7955,.T.);
#10859=ORIENTED_EDGE('',*,*,#7958,.F.);
#10860=ORIENTED_EDGE('',*,*,#7959,.F.);
#10861=ORIENTED_EDGE('',*,*,#7960,.T.);
#10862=ORIENTED_EDGE('',*,*,#7957,.T.);
#10863=ORIENTED_EDGE('',*,*,#7960,.F.);
#10864=ORIENTED_EDGE('',*,*,#7959,.T.);
#11896=CYLINDRICAL_SURFACE('',#13993,0.1954);
#12425=ADVANCED_FACE('',(#1816),#1229,.F.);
#12426=ADVANCED_FACE('',(#1817),#1230,.F.);
#12427=ADVANCED_FACE('',(#1818),#1231,.F.);
#12428=ADVANCED_FACE('',(#1819),#1232,.F.);
#12429=ADVANCED_FACE('',(#1820),#1233,.F.);
#12430=ADVANCED_FACE('',(#1821),#1234,.F.);
#12431=ADVANCED_FACE('',(#1822),#1235,.F.);
#12432=ADVANCED_FACE('',(#1823,#854),#1236,.T.);
#12433=ADVANCED_FACE('',(#1824),#481,.T.);
#12434=ADVANCED_FACE('',(#1825),#11896,.T.);
#12435=ADVANCED_FACE('',(#1826),#482,.T.);
#12436=ADVANCED_FACE('',(#1827),#1237,.T.);
#12673=CLOSED_SHELL('',(#12425,#12426,#12427,#12428,#12429,#12430,#12431,
#12432,#12433,#12434,#12435,#12436));
#13981=AXIS2_PLACEMENT_3D('',#21005,#16833,#16834);
#13982=AXIS2_PLACEMENT_3D('',#21006,#16835,#16836);
#13983=AXIS2_PLACEMENT_3D('',#21015,#16841,#16842);
#13984=AXIS2_PLACEMENT_3D('',#21021,#16846,#16847);
#13985=AXIS2_PLACEMENT_3D('',#21027,#16851,#16852);
#13986=AXIS2_PLACEMENT_3D('',#21033,#16856,#16857);
#13987=AXIS2_PLACEMENT_3D('',#21039,#16861,#16862);
#13988=AXIS2_PLACEMENT_3D('',#21042,#16865,#16866);
#13989=AXIS2_PLACEMENT_3D('',#21043,#16867,#16868);
#13990=AXIS2_PLACEMENT_3D('',#21045,#16869,#16870);
#13991=AXIS2_PLACEMENT_3D('',#21046,#16871,#16872);
#13992=AXIS2_PLACEMENT_3D('',#21048,#16873,#16874);
#13993=AXIS2_PLACEMENT_3D('',#21050,#16876,#16877);
#13994=AXIS2_PLACEMENT_3D('',#21052,#16878,#16879);
#13995=AXIS2_PLACEMENT_3D('',#21054,#16881,#16882);
#13996=AXIS2_PLACEMENT_3D('',#21056,#16883,#16884);
#13997=AXIS2_PLACEMENT_3D('',#21058,#16886,#16887);
#16833=DIRECTION('axis',(0.,0.,1.));
#16834=DIRECTION('refdir',(1.,0.,0.));
#16835=DIRECTION('center_axis',(0.866025403784439,0.,-0.5));
#16836=DIRECTION('ref_axis',(0.5,0.,0.866025403784439));
#16837=DIRECTION('',(0.5,0.,0.866025403784439));
#16838=DIRECTION('',(0.,-1.,0.));
#16839=DIRECTION('',(0.5,0.,0.866025403784439));
#16840=DIRECTION('',(0.,-1.,0.));
#16841=DIRECTION('center_axis',(1.20185167898973E-16,0.,-1.));
#16842=DIRECTION('ref_axis',(1.,0.,1.20185167898973E-16));
#16843=DIRECTION('',(1.,0.,1.20185167898973E-16));
#16844=DIRECTION('',(0.,-1.,0.));
#16845=DIRECTION('',(1.,0.,1.20185167898973E-16));
#16846=DIRECTION('center_axis',(-0.866025403784439,0.,-0.5));
#16847=DIRECTION('ref_axis',(0.5,0.,-0.866025403784439));
#16848=DIRECTION('',(0.5,0.,-0.866025403784439));
#16849=DIRECTION('',(0.,-1.,0.));
#16850=DIRECTION('',(0.5,0.,-0.866025403784439));
#16851=DIRECTION('center_axis',(-0.866025403784439,0.,0.5));
#16852=DIRECTION('ref_axis',(-0.5,0.,-0.866025403784439));
#16853=DIRECTION('',(-0.5,0.,-0.866025403784439));
#16854=DIRECTION('',(0.,-1.,0.));
#16855=DIRECTION('',(-0.5,0.,-0.866025403784439));
#16856=DIRECTION('center_axis',(-2.40370335797945E-16,0.,1.));
#16857=DIRECTION('ref_axis',(-1.,0.,-2.40370335797945E-16));
#16858=DIRECTION('',(-1.,0.,-2.40370335797945E-16));
#16859=DIRECTION('',(0.,-1.,0.));
#16860=DIRECTION('',(-1.,0.,-2.40370335797945E-16));
#16861=DIRECTION('center_axis',(0.866025403784439,0.,0.5));
#16862=DIRECTION('ref_axis',(-0.5,0.,0.866025403784439));
#16863=DIRECTION('',(-0.5,0.,0.866025403784439));
#16864=DIRECTION('',(-0.5,0.,0.866025403784439));
#16865=DIRECTION('center_axis',(0.,-1.,0.));
#16866=DIRECTION('ref_axis',(0.,0.,-1.));
#16867=DIRECTION('center_axis',(0.,1.,0.));
#16868=DIRECTION('ref_axis',(0.,0.,1.));
#16869=DIRECTION('center_axis',(0.,-1.,0.));
#16870=DIRECTION('ref_axis',(1.,0.,0.));
#16871=DIRECTION('center_axis',(0.,-1.,0.));
#16872=DIRECTION('ref_axis',(1.,0.,0.));
#16873=DIRECTION('center_axis',(0.,-1.,0.));
#16874=DIRECTION('ref_axis',(1.,0.,0.));
#16875=DIRECTION('',(0.707106781186548,0.707106781186547,8.65956056235494E-17));
#16876=DIRECTION('center_axis',(0.,-1.,0.));
#16877=DIRECTION('ref_axis',(1.,0.,0.));
#16878=DIRECTION('center_axis',(0.,1.,0.));
#16879=DIRECTION('ref_axis',(1.,0.,0.));
#16880=DIRECTION('',(0.,1.,0.));
#16881=DIRECTION('center_axis',(0.,1.,0.));
#16882=DIRECTION('ref_axis',(1.,0.,0.));
#16883=DIRECTION('center_axis',(0.,-1.,0.));
#16884=DIRECTION('ref_axis',(1.,0.,0.));
#16885=DIRECTION('',(-0.707106781186548,0.707106781186547,-8.65956056235494E-17));
#16886=DIRECTION('center_axis',(0.,-1.,0.));
#16887=DIRECTION('ref_axis',(0.,0.,-1.));
#21005=CARTESIAN_POINT('',(0.,0.,0.));
#21006=CARTESIAN_POINT('Origin',(0.0577350269189626,0.,-0.1));
#21007=CARTESIAN_POINT('',(0.0577350269189626,0.,-0.1));
#21008=CARTESIAN_POINT('',(0.115470053837925,0.,0.));
#21009=CARTESIAN_POINT('',(0.0934187836487032,0.,-0.0381939203391614));
#21010=CARTESIAN_POINT('',(0.0577350269189626,-0.2,-0.1));
#21011=CARTESIAN_POINT('',(0.0577350269189626,0.,-0.1));
#21012=CARTESIAN_POINT('',(0.115470053837925,-0.2,0.));
#21013=CARTESIAN_POINT('',(0.115470053837925,-0.2,0.));
#21014=CARTESIAN_POINT('',(0.115470053837925,0.,0.));
#21015=CARTESIAN_POINT('Origin',(-0.0577350269189626,0.,-0.1));
#21016=CARTESIAN_POINT('',(-0.0577350269189626,0.,-0.1));
#21017=CARTESIAN_POINT('',(0.0561324865405187,0.,-0.1));
#21018=CARTESIAN_POINT('',(-0.0577350269189626,-0.2,-0.1));
#21019=CARTESIAN_POINT('',(-0.0577350269189626,0.,-0.1));
#21020=CARTESIAN_POINT('',(0.0577350269189626,-0.2,-0.1));
#21021=CARTESIAN_POINT('Origin',(-0.115470053837925,0.,-1.38777878078145E-17));
#21022=CARTESIAN_POINT('',(-0.115470053837925,0.,-1.41410031829988E-17));
#21023=CARTESIAN_POINT('',(-0.0797862971081845,0.,-0.0618060796608387));
#21024=CARTESIAN_POINT('',(-0.115470053837925,-0.2,-1.38777878078145E-17));
#21025=CARTESIAN_POINT('',(-0.115470053837925,0.,-1.41410031829988E-17));
#21026=CARTESIAN_POINT('',(-0.0577350269189626,-0.2,-0.1));
#21027=CARTESIAN_POINT('Origin',(-0.0577350269189626,0.,0.1));
#21028=CARTESIAN_POINT('',(-0.0577350269189626,0.,0.1));
#21029=CARTESIAN_POINT('',(-0.0509187836487033,0.,0.111806079660839));
#21030=CARTESIAN_POINT('',(-0.0577350269189626,-0.2,0.1));
#21031=CARTESIAN_POINT('',(-0.0577350269189626,0.,0.1));
#21032=CARTESIAN_POINT('',(-0.115470053837925,-0.2,-1.41410031829988E-17));
#21033=CARTESIAN_POINT('Origin',(0.0577350269189626,0.,0.1));
#21034=CARTESIAN_POINT('',(0.0577350269189626,0.,0.1));
#21035=CARTESIAN_POINT('',(0.113867513459481,0.,0.1));
#21036=CARTESIAN_POINT('',(0.0577350269189626,-0.2,0.1));
#21037=CARTESIAN_POINT('',(0.0577350269189626,0.,0.1));
#21038=CARTESIAN_POINT('',(-0.0577350269189626,-0.2,0.1));
#21039=CARTESIAN_POINT('Origin',(0.115470053837925,0.,0.));
#21040=CARTESIAN_POINT('',(0.122286297108185,0.,-0.0118060796608386));
#21041=CARTESIAN_POINT('',(0.0577350269189626,-0.2,0.1));
#21042=CARTESIAN_POINT('Origin',(0.,-0.2,0.));
#21043=CARTESIAN_POINT('Origin',(0.17,0.,0.));
#21044=CARTESIAN_POINT('',(-0.17,-8.67361737988404E-18,-2.0818995585505E-17));
#21045=CARTESIAN_POINT('Origin',(0.,0.,0.));
#21046=CARTESIAN_POINT('Origin',(0.,-0.015,0.));
#21047=CARTESIAN_POINT('',(-0.1954,-0.0254,-2.39295984553393E-17));
#21048=CARTESIAN_POINT('Origin',(0.,-0.0254,0.));
#21049=CARTESIAN_POINT('',(-0.185,-0.015,-2.2655965784226E-17));
#21050=CARTESIAN_POINT('Origin',(0.,-0.2775,0.));
#21051=CARTESIAN_POINT('',(-0.1954,-0.5296,2.39295984553393E-17));
#21052=CARTESIAN_POINT('Origin',(0.,-0.5296,0.));
#21053=CARTESIAN_POINT('',(-0.1954,-0.2775,-2.39295984553393E-17));
#21054=CARTESIAN_POINT('Origin',(0.,-0.5625,0.));
#21055=CARTESIAN_POINT('',(-0.125,-0.6,-1.53080849893419E-17));
#21056=CARTESIAN_POINT('Origin',(0.,-0.6,0.));
#21057=CARTESIAN_POINT('',(-0.1625,-0.5625,-1.99005104861445E-17));
#21058=CARTESIAN_POINT('Origin',(0.,-0.6,0.));
#33228=UNCERTAINTY_MEASURE_WITH_UNIT(LENGTH_MEASURE(0.001),#33300,
'DISTANCE_ACCURACY_VALUE',
'Maximum model space distance between geometric entities at asserted c
onnectivities');
#33247=UNCERTAINTY_MEASURE_WITH_UNIT(LENGTH_MEASURE(0.001),#33300,
'DISTANCE_ACCURACY_VALUE',
'Maximum model space distance between geometric entities at asserted c
onnectivities');
#33280=(
GEOMETRIC_REPRESENTATION_CONTEXT(3)
GLOBAL_UNCERTAINTY_ASSIGNED_CONTEXT((#33228))
GLOBAL_UNIT_ASSIGNED_CONTEXT((#33300,#33302,#33303))
REPRESENTATION_CONTEXT('','3D')
);
#33299=(
GEOMETRIC_REPRESENTATION_CONTEXT(3)
GLOBAL_UNCERTAINTY_ASSIGNED_CONTEXT((#33247))
GLOBAL_UNIT_ASSIGNED_CONTEXT((#33300,#33302,#33303))
REPRESENTATION_CONTEXT('','3D')
);
#33300=(
LENGTH_UNIT()
NAMED_UNIT(*)
SI_UNIT(.CENTI.,.METRE.)
);
#33302=(
NAMED_UNIT(*)
PLANE_ANGLE_UNIT()
SI_UNIT($,.RADIAN.)
);
#33303=(
NAMED_UNIT(*)
SI_UNIT($,.STERADIAN.)
SOLID_ANGLE_UNIT()
);
#33336=SHAPE_DEFINITION_REPRESENTATION(#33392,#33518);
#33392=PRODUCT_DEFINITION_SHAPE('',$,#33570);
#33518=SHAPE_REPRESENTATION('',(#13981),#33280);
#33537=PRODUCT_DEFINITION_CONTEXT('part definition',#33692,'design');
#33570=PRODUCT_DEFINITION('Socket Set Screw - M4x6',
'Socket Set Screw - M4x6',#33621,#33537);
#33621=PRODUCT_DEFINITION_FORMATION('',$,#33726);
#33692=APPLICATION_CONTEXT(
'Core Data for Automotive Mechanical Design Process');
#33693=PRODUCT_CONTEXT('part definition',#33692,'mechanical');
#33726=PRODUCT('Socket Set Screw - M4x6','Socket Set Screw - M4x6',
'Socket Set Screw - M4x6',(#33693));
#33815=COLOUR_RGB('Black',0.12,0.14,0.17);
#33816=FILL_AREA_STYLE_COLOUR('',#33815);
#33817=FILL_AREA_STYLE('',(#33816));
#33818=SURFACE_STYLE_FILL_AREA(#33817);
#33819=SURFACE_SIDE_STYLE('',(#33818));
#33820=SURFACE_STYLE_USAGE(.BOTH.,#33819);
#33821=PRESENTATION_STYLE_ASSIGNMENT((#33820));
ENDSEC;
END-ISO-10303-21;
